ISO-10303-21;
HEADER;
/* Generated by software containing ST-Developer
 * from STEP Tools, Inc. (www.steptools.com) 
 */

FILE_DESCRIPTION(
/* description */ ('STEP AP214'),
/* implementation_level */ '2;1');

FILE_NAME(
/* name */ 'Low Head Cap Screw M5x25.step',
/* time_stamp */ '2026-11-15T14:55:55-08:00',
/* author */ (''),
/* organization */ (''),
/* preprocessor_version */ 'ST-DEVELOPER v20.2',
/* originating_system */ 'Autodesk Translation Framework v15.17.0.0',
/* authorisation */ '');

FILE_SCHEMA (('AUTOMOTIVE_DESIGN { 1 0 10303 214 3 1 1 }'));
ENDSEC;

DATA;
#10=MECHANICAL_DESIGN_GEOMETRIC_PRESENTATION_REPRESENTATION('',(#954,#955,#956),#57079);
#892=SHAPE_REPRESENTATION_RELATIONSHIP('SRR','None',#57282,#921);
#921=ADVANCED_BREP_SHAPE_REPRESENTATION('',(#991,#992,#993),#57074);
#954=STYLED_ITEM('',(#57444),#991);
#955=STYLED_ITEM('',(#57444),#992);
#956=STYLED_ITEM('',(#57444),#993);
#991=MANIFOLD_SOLID_BREP('Body1',#24554);
#992=MANIFOLD_SOLID_BREP('Body2',#24555);
#993=MANIFOLD_SOLID_BREP('Body3',#24556);
#1326=FACE_BOUND('',#5137,.T.);
#1327=FACE_BOUND('',#5140,.T.);
#1328=FACE_BOUND('',#5142,.T.);
#1329=FACE_BOUND('',#5158,.T.);
#1330=FACE_BOUND('',#5160,.T.);
#2031=PLANE('',#27259);
#2032=PLANE('',#27260);
#2033=PLANE('',#27261);
#2034=PLANE('',#27262);
#2035=PLANE('',#27263);
#2036=PLANE('',#27264);
#2037=PLANE('',#27265);
#2038=PLANE('',#27266);
#2039=PLANE('',#27267);
#2040=PLANE('',#27268);
#2041=PLANE('',#27269);
#2042=PLANE('',#27270);
#2043=PLANE('',#27271);
#2044=PLANE('',#27272);
#2045=PLANE('',#27273);
#2046=PLANE('',#27274);
#2047=PLANE('',#27281);
#2048=PLANE('',#27282);
#2049=PLANE('',#27289);
#2050=PLANE('',#27290);
#2051=PLANE('',#27291);
#2052=PLANE('',#27292);
#2149=CONICAL_SURFACE('',#27239,3.75,0.785398163397444);
#2150=CONICAL_SURFACE('',#27243,1664.2794823505,1.02974425867665);
#3430=FACE_OUTER_BOUND('',#5131,.T.);
#3431=FACE_OUTER_BOUND('',#5132,.T.);
#3432=FACE_OUTER_BOUND('',#5133,.T.);
#3433=FACE_OUTER_BOUND('',#5134,.T.);
#3434=FACE_OUTER_BOUND('',#5135,.T.);
#3435=FACE_OUTER_BOUND('',#5136,.T.);
#3436=FACE_OUTER_BOUND('',#5138,.T.);
#3437=FACE_OUTER_BOUND('',#5139,.T.);
#3438=FACE_OUTER_BOUND('',#5141,.T.);
#3439=FACE_OUTER_BOUND('',#5143,.T.);
#3440=FACE_OUTER_BOUND('',#5144,.T.);
#3441=FACE_OUTER_BOUND('',#5145,.T.);
#3442=FACE_OUTER_BOUND('',#5146,.T.);
#3443=FACE_OUTER_BOUND('',#5147,.T.);
#3444=FACE_OUTER_BOUND('',#5148,.T.);
#3445=FACE_OUTER_BOUND('',#5149,.T.);
#3446=FACE_OUTER_BOUND('',#5150,.T.);
#3447=FACE_OUTER_BOUND('',#5151,.T.);
#3448=FACE_OUTER_BOUND('',#5152,.T.);
#3449=FACE_OUTER_BOUND('',#5153,.T.);
#3450=FACE_OUTER_BOUND('',#5154,.T.);
#3451=FACE_OUTER_BOUND('',#5155,.T.);
#3452=FACE_OUTER_BOUND('',#5156,.T.);
#3453=FACE_OUTER_BOUND('',#5157,.T.);
#3454=FACE_OUTER_BOUND('',#5159,.T.);
#3455=FACE_OUTER_BOUND('',#5161,.T.);
#3456=FACE_OUTER_BOUND('',#5162,.T.);
#3457=FACE_OUTER_BOUND('',#5163,.T.);
#3458=FACE_OUTER_BOUND('',#5164,.T.);
#3459=FACE_OUTER_BOUND('',#5165,.T.);
#3460=FACE_OUTER_BOUND('',#5166,.T.);
#5131=EDGE_LOOP('',(#22320,#22321,#22322,#22323,#22324));
#5132=EDGE_LOOP('',(#22325,#22326,#22327,#22328,#22329,#22330,#22331,#22332,
#22333));
#5133=EDGE_LOOP('',(#22334,#22335,#22336,#22337,#22338));
#5134=EDGE_LOOP('',(#22339,#22340,#22341,#22342));
#5135=EDGE_LOOP('',(#22343,#22344,#22345,#22346));
#5136=EDGE_LOOP('',(#22347));
#5137=EDGE_LOOP('',(#22348,#22349,#22350,#22351,#22352,#22353));
#5138=EDGE_LOOP('',(#22354));
#5139=EDGE_LOOP('',(#22355));
#5140=EDGE_LOOP('',(#22356));
#5141=EDGE_LOOP('',(#22357));
#5142=EDGE_LOOP('',(#22358));
#5143=EDGE_LOOP('',(#22359,#22360,#22361,#22362,#22363));
#5144=EDGE_LOOP('',(#22364,#22365,#22366,#22367,#22368));
#5145=EDGE_LOOP('',(#22369,#22370,#22371,#22372,#22373));
#5146=EDGE_LOOP('',(#22374,#22375,#22376,#22377,#22378));
#5147=EDGE_LOOP('',(#22379,#22380,#22381,#22382,#22383));
#5148=EDGE_LOOP('',(#22384,#22385,#22386,#22387,#22388));
#5149=EDGE_LOOP('',(#22389,#22390,#22391));
#5150=EDGE_LOOP('',(#22392,#22393,#22394,#22395));
#5151=EDGE_LOOP('',(#22396,#22397,#22398));
#5152=EDGE_LOOP('',(#22399,#22400,#22401));
#5153=EDGE_LOOP('',(#22402,#22403,#22404));
#5154=EDGE_LOOP('',(#22405,#22406,#22407));
#5155=EDGE_LOOP('',(#22408,#22409,#22410,#22411));
#5156=EDGE_LOOP('',(#22412,#22413,#22414,#22415));
#5157=EDGE_LOOP('',(#22416));
#5158=EDGE_LOOP('',(#22417));
#5159=EDGE_LOOP('',(#22418));
#5160=EDGE_LOOP('',(#22419));
#5161=EDGE_LOOP('',(#22420,#22421,#22422,#22423));
#5162=EDGE_LOOP('',(#22424,#22425,#22426,#22427));
#5163=EDGE_LOOP('',(#22428,#22429,#22430,#22431));
#5164=EDGE_LOOP('',(#22432,#22433,#22434,#22435));
#5165=EDGE_LOOP('',(#22436,#22437,#22438,#22439));
#5166=EDGE_LOOP('',(#22440,#22441,#22442,#22443));
#7074=LINE('',#56489,#9041);
#7075=LINE('',#56494,#9042);
#7076=LINE('',#56510,#9043);
#7077=LINE('',#56516,#9044);
#7078=LINE('',#56522,#9045);
#7079=LINE('',#56527,#9046);
#7080=LINE('',#56529,#9047);
#7081=LINE('',#56531,#9048);
#7082=LINE('',#56533,#9049);
#7083=LINE('',#56535,#9050);
#7084=LINE('',#56536,#9051);
#7085=LINE('',#56542,#9052);
#7086=LINE('',#56543,#9053);
#7087=LINE('',#56545,#9054);
#7088=LINE('',#56546,#9055);
#7089=LINE('',#56549,#9056);
#7090=LINE('',#56550,#9057);
#7091=LINE('',#56551,#9058);
#7092=LINE('',#56554,#9059);
#7093=LINE('',#56555,#9060);
#7094=LINE('',#56556,#9061);
#7095=LINE('',#56559,#9062);
#7096=LINE('',#56560,#9063);
#7097=LINE('',#56561,#9064);
#7098=LINE('',#56564,#9065);
#7099=LINE('',#56565,#9066);
#7100=LINE('',#56566,#9067);
#7101=LINE('',#56568,#9068);
#7102=LINE('',#56569,#9069);
#7103=LINE('',#56580,#9070);
#7104=LINE('',#56586,#9071);
#7105=LINE('',#56595,#9072);
#7106=LINE('',#56598,#9073);
#7107=LINE('',#56604,#9074);
#7108=LINE('',#56607,#9075);
#7109=LINE('',#56609,#9076);
#7110=LINE('',#56610,#9077);
#7111=LINE('',#56612,#9078);
#7112=LINE('',#56613,#9079);
#9041=VECTOR('',#34018,3.75);
#9042=VECTOR('',#34023,1664.2794823505);
#9043=VECTOR('',#34040,4.25);
#9044=VECTOR('',#34047,2.065);
#9045=VECTOR('',#34054,2.5);
#9046=VECTOR('',#34059,1000.);
#9047=VECTOR('',#34060,1000.);
#9048=VECTOR('',#34061,1000.);
#9049=VECTOR('',#34062,1000.);
#9050=VECTOR('',#34063,1000.);
#9051=VECTOR('',#34064,1000.);
#9052=VECTOR('',#34073,1000.);
#9053=VECTOR('',#34074,1000.);
#9054=VECTOR('',#34075,1000.);
#9055=VECTOR('',#34076,1000.);
#9056=VECTOR('',#34079,1000.);
#9057=VECTOR('',#34080,1000.);
#9058=VECTOR('',#34081,1000.);
#9059=VECTOR('',#34084,1000.);
#9060=VECTOR('',#34085,1000.);
#9061=VECTOR('',#34086,1000.);
#9062=VECTOR('',#34089,1000.);
#9063=VECTOR('',#34090,1000.);
#9064=VECTOR('',#34091,1000.);
#9065=VECTOR('',#34094,1000.);
#9066=VECTOR('',#34095,1000.);
#9067=VECTOR('',#34096,1000.);
#9068=VECTOR('',#34099,1000.);
#9069=VECTOR('',#34100,1000.);
#9070=VECTOR('',#34117,5.);
#9071=VECTOR('',#34124,2.5);
#9072=VECTOR('',#34135,1000.);
#9073=VECTOR('',#34138,1000.);
#9074=VECTOR('',#34143,1000.);
#9075=VECTOR('',#34146,1000.);
#9076=VECTOR('',#34149,1000.);
#9077=VECTOR('',#34150,1000.);
#9078=VECTOR('',#34153,1000.);
#9079=VECTOR('',#34154,1000.);
#10212=CIRCLE('',#27240,4.25);
#10213=CIRCLE('',#27241,4.25);
#10214=CIRCLE('',#27242,3.75);
#10215=CIRCLE('',#27244,2.);
#10216=CIRCLE('',#27245,2.);
#10217=CIRCLE('',#27246,2.);
#10218=CIRCLE('',#27247,2.);
#10219=CIRCLE('',#27248,2.);
#10220=CIRCLE('',#27249,2.);
#10221=CIRCLE('',#27250,2.);
#10222=CIRCLE('',#27252,4.25);
#10223=CIRCLE('',#27254,2.065);
#10224=CIRCLE('',#27255,2.065);
#10225=CIRCLE('',#27257,2.5);
#10226=CIRCLE('',#27258,2.5);
#10227=CIRCLE('',#27276,5.);
#10228=CIRCLE('',#27277,5.);
#10229=CIRCLE('',#27279,2.5);
#10230=CIRCLE('',#27280,2.5);
#10231=CIRCLE('',#27284,4.25);
#10232=CIRCLE('',#27285,4.25);
#10233=CIRCLE('',#27287,2.5);
#10234=CIRCLE('',#27288,2.5);
#12366=VERTEX_POINT('',#56484);
#12367=VERTEX_POINT('',#56485);
#12368=VERTEX_POINT('',#56488);
#12369=VERTEX_POINT('',#56492);
#12370=VERTEX_POINT('',#56493);
#12371=VERTEX_POINT('',#56495);
#12372=VERTEX_POINT('',#56497);
#12373=VERTEX_POINT('',#56499);
#12374=VERTEX_POINT('',#56501);
#12375=VERTEX_POINT('',#56503);
#12376=VERTEX_POINT('',#56505);
#12377=VERTEX_POINT('',#56509);
#12378=VERTEX_POINT('',#56513);
#12379=VERTEX_POINT('',#56515);
#12380=VERTEX_POINT('',#56519);
#12381=VERTEX_POINT('',#56521);
#12382=VERTEX_POINT('',#56525);
#12383=VERTEX_POINT('',#56526);
#12384=VERTEX_POINT('',#56528);
#12385=VERTEX_POINT('',#56530);
#12386=VERTEX_POINT('',#56532);
#12387=VERTEX_POINT('',#56534);
#12388=VERTEX_POINT('',#56541);
#12389=VERTEX_POINT('',#56544);
#12390=VERTEX_POINT('',#56548);
#12391=VERTEX_POINT('',#56553);
#12392=VERTEX_POINT('',#56558);
#12393=VERTEX_POINT('',#56563);
#12394=VERTEX_POINT('',#56577);
#12395=VERTEX_POINT('',#56579);
#12396=VERTEX_POINT('',#56583);
#12397=VERTEX_POINT('',#56585);
#12398=VERTEX_POINT('',#56591);
#12399=VERTEX_POINT('',#56592);
#12400=VERTEX_POINT('',#56594);
#12401=VERTEX_POINT('',#56596);
#12402=VERTEX_POINT('',#56600);
#12403=VERTEX_POINT('',#56601);
#12404=VERTEX_POINT('',#56603);
#12405=VERTEX_POINT('',#56605);
#15705=EDGE_CURVE('',#12366,#12367,#10212,.T.);
#15706=EDGE_CURVE('',#12367,#12366,#10213,.T.);
#15707=EDGE_CURVE('',#12367,#12368,#7074,.T.);
#15708=EDGE_CURVE('',#12368,#12368,#10214,.T.);
#15709=EDGE_CURVE('',#12369,#12370,#7075,.T.);
#15710=EDGE_CURVE('',#12370,#12371,#10215,.T.);
#15711=EDGE_CURVE('',#12371,#12372,#10216,.T.);
#15712=EDGE_CURVE('',#12372,#12373,#10217,.T.);
#15713=EDGE_CURVE('',#12373,#12374,#10218,.T.);
#15714=EDGE_CURVE('',#12374,#12375,#10219,.T.);
#15715=EDGE_CURVE('',#12375,#12376,#10220,.T.);
#15716=EDGE_CURVE('',#12376,#12370,#10221,.T.);
#15717=EDGE_CURVE('',#12366,#12377,#7076,.T.);
#15718=EDGE_CURVE('',#12377,#12377,#10222,.T.);
#15719=EDGE_CURVE('',#12378,#12378,#10223,.T.);
#15720=EDGE_CURVE('',#12378,#12379,#7077,.T.);
#15721=EDGE_CURVE('',#12379,#12379,#10224,.T.);
#15722=EDGE_CURVE('',#12380,#12380,#10225,.T.);
#15723=EDGE_CURVE('',#12380,#12381,#7078,.T.);
#15724=EDGE_CURVE('',#12381,#12381,#10226,.T.);
#15725=EDGE_CURVE('',#12382,#12383,#7079,.T.);
#15726=EDGE_CURVE('',#12384,#12382,#7080,.T.);
#15727=EDGE_CURVE('',#12385,#12384,#7081,.T.);
#15728=EDGE_CURVE('',#12386,#12385,#7082,.T.);
#15729=EDGE_CURVE('',#12387,#12386,#7083,.T.);
#15730=EDGE_CURVE('',#12383,#12387,#7084,.T.);
#15731=EDGE_CURVE('',#12388,#12375,#7085,.T.);
#15732=EDGE_CURVE('',#12388,#12384,#7086,.T.);
#15733=EDGE_CURVE('',#12389,#12382,#7087,.T.);
#15734=EDGE_CURVE('',#12375,#12389,#7088,.T.);
#15735=EDGE_CURVE('',#12390,#12374,#7089,.T.);
#15736=EDGE_CURVE('',#12390,#12385,#7090,.T.);
#15737=EDGE_CURVE('',#12374,#12388,#7091,.T.);
#15738=EDGE_CURVE('',#12391,#12373,#7092,.T.);
#15739=EDGE_CURVE('',#12391,#12386,#7093,.T.);
#15740=EDGE_CURVE('',#12373,#12390,#7094,.T.);
#15741=EDGE_CURVE('',#12392,#12372,#7095,.T.);
#15742=EDGE_CURVE('',#12392,#12387,#7096,.T.);
#15743=EDGE_CURVE('',#12372,#12391,#7097,.T.);
#15744=EDGE_CURVE('',#12393,#12371,#7098,.T.);
#15745=EDGE_CURVE('',#12393,#12383,#7099,.T.);
#15746=EDGE_CURVE('',#12371,#12392,#7100,.T.);
#15747=EDGE_CURVE('',#12389,#12376,#7101,.T.);
#15748=EDGE_CURVE('',#12376,#12393,#7102,.T.);
#15749=EDGE_CURVE('',#12394,#12394,#10227,.T.);
#15750=EDGE_CURVE('',#12394,#12395,#7103,.T.);
#15751=EDGE_CURVE('',#12395,#12395,#10228,.T.);
#15752=EDGE_CURVE('',#12396,#12396,#10229,.T.);
#15753=EDGE_CURVE('',#12396,#12397,#7104,.T.);
#15754=EDGE_CURVE('',#12397,#12397,#10230,.T.);
#15755=EDGE_CURVE('',#12398,#12399,#10231,.T.);
#15756=EDGE_CURVE('',#12400,#12399,#7105,.T.);
#15757=EDGE_CURVE('',#12401,#12400,#10232,.T.);
#15758=EDGE_CURVE('',#12401,#12398,#7106,.T.);
#15759=EDGE_CURVE('',#12402,#12403,#10233,.T.);
#15760=EDGE_CURVE('',#12404,#12402,#7107,.T.);
#15761=EDGE_CURVE('',#12404,#12405,#10234,.T.);
#15762=EDGE_CURVE('',#12405,#12403,#7108,.T.);
#15763=EDGE_CURVE('',#12400,#12405,#7109,.T.);
#15764=EDGE_CURVE('',#12404,#12401,#7110,.T.);
#15765=EDGE_CURVE('',#12399,#12403,#7111,.T.);
#15766=EDGE_CURVE('',#12402,#12398,#7112,.T.);
#22320=ORIENTED_EDGE('',*,*,#15705,.F.);
#22321=ORIENTED_EDGE('',*,*,#15706,.F.);
#22322=ORIENTED_EDGE('',*,*,#15707,.T.);
#22323=ORIENTED_EDGE('',*,*,#15708,.F.);
#22324=ORIENTED_EDGE('',*,*,#15707,.F.);
#22325=ORIENTED_EDGE('',*,*,#15709,.T.);
#22326=ORIENTED_EDGE('',*,*,#15710,.T.);
#22327=ORIENTED_EDGE('',*,*,#15711,.T.);
#22328=ORIENTED_EDGE('',*,*,#15712,.T.);
#22329=ORIENTED_EDGE('',*,*,#15713,.T.);
#22330=ORIENTED_EDGE('',*,*,#15714,.T.);
#22331=ORIENTED_EDGE('',*,*,#15715,.T.);
#22332=ORIENTED_EDGE('',*,*,#15716,.T.);
#22333=ORIENTED_EDGE('',*,*,#15709,.F.);
#22334=ORIENTED_EDGE('',*,*,#15705,.T.);
#22335=ORIENTED_EDGE('',*,*,#15706,.T.);
#22336=ORIENTED_EDGE('',*,*,#15717,.T.);
#22337=ORIENTED_EDGE('',*,*,#15718,.T.);
#22338=ORIENTED_EDGE('',*,*,#15717,.F.);
#22339=ORIENTED_EDGE('',*,*,#15719,.F.);
#22340=ORIENTED_EDGE('',*,*,#15720,.T.);
#22341=ORIENTED_EDGE('',*,*,#15721,.T.);
#22342=ORIENTED_EDGE('',*,*,#15720,.F.);
#22343=ORIENTED_EDGE('',*,*,#15722,.F.);
#22344=ORIENTED_EDGE('',*,*,#15723,.T.);
#22345=ORIENTED_EDGE('',*,*,#15724,.T.);
#22346=ORIENTED_EDGE('',*,*,#15723,.F.);
#22347=ORIENTED_EDGE('',*,*,#15708,.T.);
#22348=ORIENTED_EDGE('',*,*,#15725,.F.);
#22349=ORIENTED_EDGE('',*,*,#15726,.F.);
#22350=ORIENTED_EDGE('',*,*,#15727,.F.);
#22351=ORIENTED_EDGE('',*,*,#15728,.F.);
#22352=ORIENTED_EDGE('',*,*,#15729,.F.);
#22353=ORIENTED_EDGE('',*,*,#15730,.F.);
#22354=ORIENTED_EDGE('',*,*,#15724,.F.);
#22355=ORIENTED_EDGE('',*,*,#15722,.T.);
#22356=ORIENTED_EDGE('',*,*,#15721,.F.);
#22357=ORIENTED_EDGE('',*,*,#15718,.F.);
#22358=ORIENTED_EDGE('',*,*,#15719,.T.);
#22359=ORIENTED_EDGE('',*,*,#15731,.F.);
#22360=ORIENTED_EDGE('',*,*,#15732,.T.);
#22361=ORIENTED_EDGE('',*,*,#15726,.T.);
#22362=ORIENTED_EDGE('',*,*,#15733,.F.);
#22363=ORIENTED_EDGE('',*,*,#15734,.F.);
#22364=ORIENTED_EDGE('',*,*,#15735,.F.);
#22365=ORIENTED_EDGE('',*,*,#15736,.T.);
#22366=ORIENTED_EDGE('',*,*,#15727,.T.);
#22367=ORIENTED_EDGE('',*,*,#15732,.F.);
#22368=ORIENTED_EDGE('',*,*,#15737,.F.);
#22369=ORIENTED_EDGE('',*,*,#15738,.F.);
#22370=ORIENTED_EDGE('',*,*,#15739,.T.);
#22371=ORIENTED_EDGE('',*,*,#15728,.T.);
#22372=ORIENTED_EDGE('',*,*,#15736,.F.);
#22373=ORIENTED_EDGE('',*,*,#15740,.F.);
#22374=ORIENTED_EDGE('',*,*,#15741,.F.);
#22375=ORIENTED_EDGE('',*,*,#15742,.T.);
#22376=ORIENTED_EDGE('',*,*,#15729,.T.);
#22377=ORIENTED_EDGE('',*,*,#15739,.F.);
#22378=ORIENTED_EDGE('',*,*,#15743,.F.);
#22379=ORIENTED_EDGE('',*,*,#15744,.F.);
#22380=ORIENTED_EDGE('',*,*,#15745,.T.);
#22381=ORIENTED_EDGE('',*,*,#15730,.T.);
#22382=ORIENTED_EDGE('',*,*,#15742,.F.);
#22383=ORIENTED_EDGE('',*,*,#15746,.F.);
#22384=ORIENTED_EDGE('',*,*,#15747,.F.);
#22385=ORIENTED_EDGE('',*,*,#15733,.T.);
#22386=ORIENTED_EDGE('',*,*,#15725,.T.);
#22387=ORIENTED_EDGE('',*,*,#15745,.F.);
#22388=ORIENTED_EDGE('',*,*,#15748,.F.);
#22389=ORIENTED_EDGE('',*,*,#15734,.T.);
#22390=ORIENTED_EDGE('',*,*,#15747,.T.);
#22391=ORIENTED_EDGE('',*,*,#15715,.F.);
#22392=ORIENTED_EDGE('',*,*,#15748,.T.);
#22393=ORIENTED_EDGE('',*,*,#15744,.T.);
#22394=ORIENTED_EDGE('',*,*,#15710,.F.);
#22395=ORIENTED_EDGE('',*,*,#15716,.F.);
#22396=ORIENTED_EDGE('',*,*,#15746,.T.);
#22397=ORIENTED_EDGE('',*,*,#15741,.T.);
#22398=ORIENTED_EDGE('',*,*,#15711,.F.);
#22399=ORIENTED_EDGE('',*,*,#15743,.T.);
#22400=ORIENTED_EDGE('',*,*,#15738,.T.);
#22401=ORIENTED_EDGE('',*,*,#15712,.F.);
#22402=ORIENTED_EDGE('',*,*,#15740,.T.);
#22403=ORIENTED_EDGE('',*,*,#15735,.T.);
#22404=ORIENTED_EDGE('',*,*,#15713,.F.);
#22405=ORIENTED_EDGE('',*,*,#15737,.T.);
#22406=ORIENTED_EDGE('',*,*,#15731,.T.);
#22407=ORIENTED_EDGE('',*,*,#15714,.F.);
#22408=ORIENTED_EDGE('',*,*,#15749,.F.);
#22409=ORIENTED_EDGE('',*,*,#15750,.T.);
#22410=ORIENTED_EDGE('',*,*,#15751,.T.);
#22411=ORIENTED_EDGE('',*,*,#15750,.F.);
#22412=ORIENTED_EDGE('',*,*,#15752,.F.);
#22413=ORIENTED_EDGE('',*,*,#15753,.T.);
#22414=ORIENTED_EDGE('',*,*,#15754,.T.);
#22415=ORIENTED_EDGE('',*,*,#15753,.F.);
#22416=ORIENTED_EDGE('',*,*,#15749,.T.);
#22417=ORIENTED_EDGE('',*,*,#15754,.F.);
#22418=ORIENTED_EDGE('',*,*,#15751,.F.);
#22419=ORIENTED_EDGE('',*,*,#15752,.T.);
#22420=ORIENTED_EDGE('',*,*,#15755,.T.);
#22421=ORIENTED_EDGE('',*,*,#15756,.F.);
#22422=ORIENTED_EDGE('',*,*,#15757,.F.);
#22423=ORIENTED_EDGE('',*,*,#15758,.T.);
#22424=ORIENTED_EDGE('',*,*,#15759,.F.);
#22425=ORIENTED_EDGE('',*,*,#15760,.F.);
#22426=ORIENTED_EDGE('',*,*,#15761,.T.);
#22427=ORIENTED_EDGE('',*,*,#15762,.T.);
#22428=ORIENTED_EDGE('',*,*,#15757,.T.);
#22429=ORIENTED_EDGE('',*,*,#15763,.T.);
#22430=ORIENTED_EDGE('',*,*,#15761,.F.);
#22431=ORIENTED_EDGE('',*,*,#15764,.T.);
#22432=ORIENTED_EDGE('',*,*,#15759,.T.);
#22433=ORIENTED_EDGE('',*,*,#15765,.F.);
#22434=ORIENTED_EDGE('',*,*,#15755,.F.);
#22435=ORIENTED_EDGE('',*,*,#15766,.F.);
#22436=ORIENTED_EDGE('',*,*,#15766,.T.);
#22437=ORIENTED_EDGE('',*,*,#15758,.F.);
#22438=ORIENTED_EDGE('',*,*,#15764,.F.);
#22439=ORIENTED_EDGE('',*,*,#15760,.T.);
#22440=ORIENTED_EDGE('',*,*,#15765,.T.);
#22441=ORIENTED_EDGE('',*,*,#15762,.F.);
#22442=ORIENTED_EDGE('',*,*,#15763,.F.);
#22443=ORIENTED_EDGE('',*,*,#15756,.T.);
#23131=CYLINDRICAL_SURFACE('',#27251,4.25);
#23132=CYLINDRICAL_SURFACE('',#27253,2.065);
#23133=CYLINDRICAL_SURFACE('',#27256,2.5);
#23134=CYLINDRICAL_SURFACE('',#27275,5.);
#23135=CYLINDRICAL_SURFACE('',#27278,2.5);
#23136=CYLINDRICAL_SURFACE('',#27283,4.25);
#23137=CYLINDRICAL_SURFACE('',#27286,2.5);
#24422=ADVANCED_FACE('',(#3430),#2149,.T.);
#24423=ADVANCED_FACE('',(#3431),#2150,.F.);
#24424=ADVANCED_FACE('',(#3432),#23131,.T.);
#24425=ADVANCED_FACE('',(#3433),#23132,.T.);
#24426=ADVANCED_FACE('',(#3434),#23133,.T.);
#24427=ADVANCED_FACE('',(#3435,#1326),#2031,.F.);
#24428=ADVANCED_FACE('',(#3436),#2032,.F.);
#24429=ADVANCED_FACE('',(#3437,#1327),#2033,.F.);
#24430=ADVANCED_FACE('',(#3438,#1328),#2034,.F.);
#24431=ADVANCED_FACE('',(#3439),#2035,.F.);
#24432=ADVANCED_FACE('',(#3440),#2036,.F.);
#24433=ADVANCED_FACE('',(#3441),#2037,.F.);
#24434=ADVANCED_FACE('',(#3442),#2038,.F.);
#24435=ADVANCED_FACE('',(#3443),#2039,.F.);
#24436=ADVANCED_FACE('',(#3444),#2040,.F.);
#24437=ADVANCED_FACE('',(#3445),#2041,.T.);
#24438=ADVANCED_FACE('',(#3446),#2042,.T.);
#24439=ADVANCED_FACE('',(#3447),#2043,.T.);
#24440=ADVANCED_FACE('',(#3448),#2044,.T.);
#24441=ADVANCED_FACE('',(#3449),#2045,.T.);
#24442=ADVANCED_FACE('',(#3450),#2046,.T.);
#24443=ADVANCED_FACE('',(#3451),#23134,.T.);
#24444=ADVANCED_FACE('',(#3452),#23135,.F.);
#24445=ADVANCED_FACE('',(#3453,#1329),#2047,.F.);
#24446=ADVANCED_FACE('',(#3454,#1330),#2048,.F.);
#24447=ADVANCED_FACE('',(#3455),#23136,.T.);
#24448=ADVANCED_FACE('',(#3456),#23137,.F.);
#24449=ADVANCED_FACE('',(#3457),#2049,.F.);
#24450=ADVANCED_FACE('',(#3458),#2050,.F.);
#24451=ADVANCED_FACE('',(#3459),#2051,.F.);
#24452=ADVANCED_FACE('',(#3460),#2052,.F.);
#24554=CLOSED_SHELL('',(#24422,#24423,#24424,#24425,#24426,#24427,#24428,
#24429,#24430,#24431,#24432,#24433,#24434,#24435,#24436,#24437,#24438,#24439,
#24440,#24441,#24442));
#24555=CLOSED_SHELL('',(#24443,#24444,#24445,#24446));
#24556=CLOSED_SHELL('',(#24447,#24448,#24449,#24450,#24451,#24452));
#27238=AXIS2_PLACEMENT_3D('',#56482,#34010,#34011);
#27239=AXIS2_PLACEMENT_3D('',#56483,#34012,#34013);
#27240=AXIS2_PLACEMENT_3D('',#56486,#34014,#34015);
#27241=AXIS2_PLACEMENT_3D('',#56487,#34016,#34017);
#27242=AXIS2_PLACEMENT_3D('',#56490,#34019,#34020);
#27243=AXIS2_PLACEMENT_3D('',#56491,#34021,#34022);
#27244=AXIS2_PLACEMENT_3D('',#56496,#34024,#34025);
#27245=AXIS2_PLACEMENT_3D('',#56498,#34026,#34027);
#27246=AXIS2_PLACEMENT_3D('',#56500,#34028,#34029);
#27247=AXIS2_PLACEMENT_3D('',#56502,#34030,#34031);
#27248=AXIS2_PLACEMENT_3D('',#56504,#34032,#34033);
#27249=AXIS2_PLACEMENT_3D('',#56506,#34034,#34035);
#27250=AXIS2_PLACEMENT_3D('',#56507,#34036,#34037);
#27251=AXIS2_PLACEMENT_3D('',#56508,#34038,#34039);
#27252=AXIS2_PLACEMENT_3D('',#56511,#34041,#34042);
#27253=AXIS2_PLACEMENT_3D('',#56512,#34043,#34044);
#27254=AXIS2_PLACEMENT_3D('',#56514,#34045,#34046);
#27255=AXIS2_PLACEMENT_3D('',#56517,#34048,#34049);
#27256=AXIS2_PLACEMENT_3D('',#56518,#34050,#34051);
#27257=AXIS2_PLACEMENT_3D('',#56520,#34052,#34053);
#27258=AXIS2_PLACEMENT_3D('',#56523,#34055,#34056);
#27259=AXIS2_PLACEMENT_3D('',#56524,#34057,#34058);
#27260=AXIS2_PLACEMENT_3D('',#56537,#34065,#34066);
#27261=AXIS2_PLACEMENT_3D('',#56538,#34067,#34068);
#27262=AXIS2_PLACEMENT_3D('',#56539,#34069,#34070);
#27263=AXIS2_PLACEMENT_3D('',#56540,#34071,#34072);
#27264=AXIS2_PLACEMENT_3D('',#56547,#34077,#34078);
#27265=AXIS2_PLACEMENT_3D('',#56552,#34082,#34083);
#27266=AXIS2_PLACEMENT_3D('',#56557,#34087,#34088);
#27267=AXIS2_PLACEMENT_3D('',#56562,#34092,#34093);
#27268=AXIS2_PLACEMENT_3D('',#56567,#34097,#34098);
#27269=AXIS2_PLACEMENT_3D('',#56570,#34101,#34102);
#27270=AXIS2_PLACEMENT_3D('',#56571,#34103,#34104);
#27271=AXIS2_PLACEMENT_3D('',#56572,#34105,#34106);
#27272=AXIS2_PLACEMENT_3D('',#56573,#34107,#34108);
#27273=AXIS2_PLACEMENT_3D('',#56574,#34109,#34110);
#27274=AXIS2_PLACEMENT_3D('',#56575,#34111,#34112);
#27275=AXIS2_PLACEMENT_3D('',#56576,#34113,#34114);
#27276=AXIS2_PLACEMENT_3D('',#56578,#34115,#34116);
#27277=AXIS2_PLACEMENT_3D('',#56581,#34118,#34119);
#27278=AXIS2_PLACEMENT_3D('',#56582,#34120,#34121);
#27279=AXIS2_PLACEMENT_3D('',#56584,#34122,#34123);
#27280=AXIS2_PLACEMENT_3D('',#56587,#34125,#34126);
#27281=AXIS2_PLACEMENT_3D('',#56588,#34127,#34128);
#27282=AXIS2_PLACEMENT_3D('',#56589,#34129,#34130);
#27283=AXIS2_PLACEMENT_3D('',#56590,#34131,#34132);
#27284=AXIS2_PLACEMENT_3D('',#56593,#34133,#34134);
#27285=AXIS2_PLACEMENT_3D('',#56597,#34136,#34137);
#27286=AXIS2_PLACEMENT_3D('',#56599,#34139,#34140);
#27287=AXIS2_PLACEMENT_3D('',#56602,#34141,#34142);
#27288=AXIS2_PLACEMENT_3D('',#56606,#34144,#34145);
#27289=AXIS2_PLACEMENT_3D('',#56608,#34147,#34148);
#27290=AXIS2_PLACEMENT_3D('',#56611,#34151,#34152);
#27291=AXIS2_PLACEMENT_3D('',#56614,#34155,#34156);
#27292=AXIS2_PLACEMENT_3D('',#56615,#34157,#34158);
#34010=DIRECTION('axis',(0.,0.,1.));
#34011=DIRECTION('refdir',(1.,0.,0.));
#34012=DIRECTION('center_axis',(1.,0.,0.));
#34013=DIRECTION('ref_axis',(0.,0.,-1.));
#34014=DIRECTION('center_axis',(1.,0.,0.));
#34015=DIRECTION('ref_axis',(0.,0.,-1.));
#34016=DIRECTION('center_axis',(1.,0.,0.));
#34017=DIRECTION('ref_axis',(0.,0.,-1.));
#34018=DIRECTION('',(-0.70710678118655,8.65956056235489E-17,-0.707106781186544));
#34019=DIRECTION('center_axis',(-1.,0.,0.));
#34020=DIRECTION('ref_axis',(0.,0.,-1.));
#34021=DIRECTION('center_axis',(-1.,5.24877093477881E-17,0.));
#34022=DIRECTION('ref_axis',(-5.24877093477881E-17,-1.,0.));
#34023=DIRECTION('',(-0.515038074910058,0.85716730070211,-1.04972719113862E-16));
#34024=DIRECTION('center_axis',(-1.,5.24877093477881E-17,0.));
#34025=DIRECTION('ref_axis',(-5.24877093477881E-17,-1.,0.));
#34026=DIRECTION('center_axis',(-1.,5.24877093477881E-17,0.));
#34027=DIRECTION('ref_axis',(-5.24877093477881E-17,-1.,0.));
#34028=DIRECTION('center_axis',(-1.,5.24877093477881E-17,0.));
#34029=DIRECTION('ref_axis',(-5.24877093477881E-17,-1.,0.));
#34030=DIRECTION('center_axis',(-1.,5.24877093477881E-17,0.));
#34031=DIRECTION('ref_axis',(-5.24877093477881E-17,-1.,0.));
#34032=DIRECTION('center_axis',(-1.,5.24877093477881E-17,0.));
#34033=DIRECTION('ref_axis',(-5.24877093477881E-17,-1.,0.));
#34034=DIRECTION('center_axis',(-1.,5.24877093477881E-17,0.));
#34035=DIRECTION('ref_axis',(-5.24877093477881E-17,-1.,0.));
#34036=DIRECTION('center_axis',(-1.,5.24877093477881E-17,0.));
#34037=DIRECTION('ref_axis',(-5.24877093477881E-17,-1.,0.));
#34038=DIRECTION('center_axis',(-1.,0.,0.));
#34039=DIRECTION('ref_axis',(0.,0.,1.));
#34040=DIRECTION('',(1.,0.,0.));
#34041=DIRECTION('center_axis',(-1.,0.,0.));
#34042=DIRECTION('ref_axis',(0.,0.,1.));
#34043=DIRECTION('center_axis',(-1.,0.,0.));
#34044=DIRECTION('ref_axis',(0.,0.,1.));
#34045=DIRECTION('center_axis',(-1.,0.,0.));
#34046=DIRECTION('ref_axis',(0.,0.,1.));
#34047=DIRECTION('',(1.,0.,0.));
#34048=DIRECTION('center_axis',(-1.,0.,0.));
#34049=DIRECTION('ref_axis',(0.,0.,1.));
#34050=DIRECTION('center_axis',(-1.,0.,0.));
#34051=DIRECTION('ref_axis',(0.,0.,1.));
#34052=DIRECTION('center_axis',(-1.,0.,0.));
#34053=DIRECTION('ref_axis',(0.,0.,1.));
#34054=DIRECTION('',(1.,0.,0.));
#34055=DIRECTION('center_axis',(-1.,0.,0.));
#34056=DIRECTION('ref_axis',(0.,0.,1.));
#34057=DIRECTION('center_axis',(1.,0.,0.));
#34058=DIRECTION('ref_axis',(0.,0.,-1.));
#34059=DIRECTION('',(0.,0.5,-0.866025403784439));
#34060=DIRECTION('',(0.,1.,-1.87789324842145E-16));
#34061=DIRECTION('',(0.,0.5,0.866025403784439));
#34062=DIRECTION('',(0.,-0.5,0.866025403784439));
#34063=DIRECTION('',(0.,-1.,0.));
#34064=DIRECTION('',(0.,-0.5,-0.866025403784439));
#34065=DIRECTION('center_axis',(-1.,0.,0.));
#34066=DIRECTION('ref_axis',(0.,0.,1.));
#34067=DIRECTION('center_axis',(1.,0.,0.));
#34068=DIRECTION('ref_axis',(0.,0.,-1.));
#34069=DIRECTION('center_axis',(-1.,0.,0.));
#34070=DIRECTION('ref_axis',(0.,0.,1.));
#34071=DIRECTION('center_axis',(0.,1.87789324842145E-16,1.));
#34072=DIRECTION('ref_axis',(0.,-1.,1.87789324842145E-16));
#34073=DIRECTION('',(0.,1.,-1.87789324842145E-16));
#34074=DIRECTION('',(-1.,0.,0.));
#34075=DIRECTION('',(-1.,0.,0.));
#34076=DIRECTION('',(0.,1.,-1.87789324842145E-16));
#34077=DIRECTION('center_axis',(0.,-0.866025403784439,0.5));
#34078=DIRECTION('ref_axis',(0.,-0.5,-0.866025403784439));
#34079=DIRECTION('',(0.,0.5,0.866025403784439));
#34080=DIRECTION('',(-1.,0.,0.));
#34081=DIRECTION('',(0.,0.5,0.866025403784439));
#34082=DIRECTION('center_axis',(0.,-0.866025403784439,-0.5));
#34083=DIRECTION('ref_axis',(0.,0.5,-0.866025403784439));
#34084=DIRECTION('',(0.,-0.5,0.866025403784439));
#34085=DIRECTION('',(-1.,0.,0.));
#34086=DIRECTION('',(0.,-0.5,0.866025403784439));
#34087=DIRECTION('center_axis',(0.,0.,-1.));
#34088=DIRECTION('ref_axis',(-1.,0.,0.));
#34089=DIRECTION('',(0.,-1.,0.));
#34090=DIRECTION('',(-1.,0.,0.));
#34091=DIRECTION('',(0.,-1.,0.));
#34092=DIRECTION('center_axis',(0.,0.866025403784439,-0.5));
#34093=DIRECTION('ref_axis',(0.,0.5,0.866025403784439));
#34094=DIRECTION('',(0.,-0.5,-0.866025403784439));
#34095=DIRECTION('',(-1.,0.,0.));
#34096=DIRECTION('',(0.,-0.5,-0.866025403784439));
#34097=DIRECTION('center_axis',(0.,0.866025403784439,0.5));
#34098=DIRECTION('ref_axis',(0.,-0.5,0.866025403784439));
#34099=DIRECTION('',(0.,0.5,-0.866025403784439));
#34100=DIRECTION('',(0.,0.5,-0.866025403784439));
#34101=DIRECTION('center_axis',(-1.,0.,0.));
#34102=DIRECTION('ref_axis',(0.,0.,1.));
#34103=DIRECTION('center_axis',(-1.,0.,0.));
#34104=DIRECTION('ref_axis',(0.,0.,1.));
#34105=DIRECTION('center_axis',(-1.,0.,0.));
#34106=DIRECTION('ref_axis',(0.,0.,1.));
#34107=DIRECTION('center_axis',(-1.,0.,0.));
#34108=DIRECTION('ref_axis',(0.,0.,1.));
#34109=DIRECTION('center_axis',(-1.,0.,0.));
#34110=DIRECTION('ref_axis',(0.,0.,1.));
#34111=DIRECTION('center_axis',(-1.,0.,0.));
#34112=DIRECTION('ref_axis',(0.,0.,1.));
#34113=DIRECTION('center_axis',(-1.,-3.84779799073557E-18,0.));
#34114=DIRECTION('ref_axis',(3.84779799073557E-18,-1.,0.));
#34115=DIRECTION('center_axis',(-1.,-3.84779799073557E-18,0.));
#34116=DIRECTION('ref_axis',(3.84779799073557E-18,-1.,0.));
#34117=DIRECTION('',(1.,3.84779799073557E-18,0.));
#34118=DIRECTION('center_axis',(-1.,-3.84779799073557E-18,0.));
#34119=DIRECTION('ref_axis',(3.84779799073557E-18,-1.,0.));
#34120=DIRECTION('center_axis',(-1.,-3.84779799073557E-18,0.));
#34121=DIRECTION('ref_axis',(3.84779799073557E-18,-1.,0.));
#34122=DIRECTION('center_axis',(-1.,-3.84779799073557E-18,0.));
#34123=DIRECTION('ref_axis',(3.84779799073557E-18,-1.,0.));
#34124=DIRECTION('',(-1.,-3.84779799073557E-18,0.));
#34125=DIRECTION('center_axis',(-1.,-3.84779799073557E-18,0.));
#34126=DIRECTION('ref_axis',(3.84779799073557E-18,-1.,0.));
#34127=DIRECTION('center_axis',(1.,3.84779799073557E-18,0.));
#34128=DIRECTION('ref_axis',(-3.84779799073557E-18,1.,0.));
#34129=DIRECTION('center_axis',(-1.,-3.84779799073557E-18,0.));
#34130=DIRECTION('ref_axis',(3.84779799073557E-18,-1.,0.));
#34131=DIRECTION('center_axis',(-1.,-1.22125762314651E-17,0.));
#34132=DIRECTION('ref_axis',(-3.62527989531715E-33,1.83697019872103E-16,
-1.));
#34133=DIRECTION('center_axis',(-1.,-1.22125762314651E-17,0.));
#34134=DIRECTION('ref_axis',(1.22125762314651E-17,-1.,0.));
#34135=DIRECTION('',(1.,0.,0.));
#34136=DIRECTION('center_axis',(-1.,-1.22125762314651E-17,0.));
#34137=DIRECTION('ref_axis',(1.22125762314651E-17,-1.,0.));
#34138=DIRECTION('',(1.,0.,0.));
#34139=DIRECTION('center_axis',(-1.,-1.22125762314651E-17,0.));
#34140=DIRECTION('ref_axis',(-3.08148791101958E-33,1.83697019872103E-16,
-1.));
#34141=DIRECTION('center_axis',(-1.,-1.22125762314651E-17,0.));
#34142=DIRECTION('ref_axis',(1.22125762314651E-17,-1.,0.));
#34143=DIRECTION('',(1.,0.,0.));
#34144=DIRECTION('center_axis',(-1.,-1.22125762314651E-17,0.));
#34145=DIRECTION('ref_axis',(1.22125762314651E-17,-1.,0.));
#34146=DIRECTION('',(1.,0.,0.));
#34147=DIRECTION('center_axis',(1.,1.22125762314651E-17,0.));
#34148=DIRECTION('ref_axis',(-1.22125762314651E-17,1.,0.));
#34149=DIRECTION('',(0.,0.,-1.));
#34150=DIRECTION('',(0.,0.,1.));
#34151=DIRECTION('center_axis',(-1.,-1.22125762314651E-17,0.));
#34152=DIRECTION('ref_axis',(1.22125762314651E-17,-1.,0.));
#34153=DIRECTION('',(0.,0.,-1.));
#34154=DIRECTION('',(0.,0.,1.));
#34155=DIRECTION('center_axis',(0.,1.,0.));
#34156=DIRECTION('ref_axis',(0.,0.,1.));
#34157=DIRECTION('center_axis',(0.,-1.,0.));
#34158=DIRECTION('ref_axis',(0.,0.,-1.));
#56482=CARTESIAN_POINT('',(0.,0.,0.));
#56483=CARTESIAN_POINT('Origin',(-7.3,0.,0.));
#56484=CARTESIAN_POINT('',(-6.79999999999999,5.20474889637625E-16,-4.25));
#56485=CARTESIAN_POINT('',(-6.79999999999999,-5.20474889637625E-16,4.25));
#56486=CARTESIAN_POINT('Origin',(-6.79999999999999,0.,0.));
#56487=CARTESIAN_POINT('Origin',(-6.79999999999999,0.,0.));
#56488=CARTESIAN_POINT('',(-7.3,-4.59242549680257E-16,3.75));
#56489=CARTESIAN_POINT('',(-7.3,-4.59242549680257E-16,3.75));
#56490=CARTESIAN_POINT('Origin',(-7.3,0.,0.));
#56491=CARTESIAN_POINT('Origin',(-1003.59827876194,5.22934144793585E-14,
0.));
#56492=CARTESIAN_POINT('',(-3.59827876194487,-1.94294868429572E-16,0.));
#56493=CARTESIAN_POINT('',(-4.80000000000004,2.00000000000045,-2.44929359829514E-16));
#56494=CARTESIAN_POINT('',(-1003.59827876194,1664.2794823505,-2.03815454094715E-13));
#56495=CARTESIAN_POINT('',(-4.8,1.73205080756888,-1.));
#56496=CARTESIAN_POINT('Origin',(-4.8,-1.3121927336947E-16,0.));
#56497=CARTESIAN_POINT('',(-4.8,-1.3121927336947E-16,-2.));
#56498=CARTESIAN_POINT('Origin',(-4.8,-1.3121927336947E-16,0.));
#56499=CARTESIAN_POINT('',(-4.8,-1.73205080756888,-1.));
#56500=CARTESIAN_POINT('Origin',(-4.8,-1.3121927336947E-16,0.));
#56501=CARTESIAN_POINT('',(-4.8,-1.73205080756888,1.));
#56502=CARTESIAN_POINT('Origin',(-4.8,-1.3121927336947E-16,0.));
#56503=CARTESIAN_POINT('',(-4.8,2.4435937631482E-16,2.));
#56504=CARTESIAN_POINT('Origin',(-4.8,-1.3121927336947E-16,0.));
#56505=CARTESIAN_POINT('',(-4.8,1.73205080756888,0.999999999999999));
#56506=CARTESIAN_POINT('Origin',(-4.8,-1.3121927336947E-16,0.));
#56507=CARTESIAN_POINT('Origin',(-4.8,-1.3121927336947E-16,0.));
#56508=CARTESIAN_POINT('Origin',(-7.3,0.,0.));
#56509=CARTESIAN_POINT('',(-2.3,-5.20474889637625E-16,-4.25));
#56510=CARTESIAN_POINT('',(-7.3,-5.20474889637625E-16,-4.25));
#56511=CARTESIAN_POINT('Origin',(-2.3,0.,0.));
#56512=CARTESIAN_POINT('Origin',(-7.3,0.,0.));
#56513=CARTESIAN_POINT('',(-2.3,-2.52889564023928E-16,-2.065));
#56514=CARTESIAN_POINT('Origin',(-2.3,0.,0.));
#56515=CARTESIAN_POINT('',(2.85,-2.52889564023928E-16,-2.065));
#56516=CARTESIAN_POINT('',(-7.3,-2.52889564023928E-16,-2.065));
#56517=CARTESIAN_POINT('Origin',(2.85,0.,0.));
#56518=CARTESIAN_POINT('Origin',(-7.3,0.,0.));
#56519=CARTESIAN_POINT('',(2.85,-3.06161699786838E-16,-2.5));
#56520=CARTESIAN_POINT('Origin',(2.85,0.,0.));
#56521=CARTESIAN_POINT('',(22.7,-3.06161699786838E-16,-2.5));
#56522=CARTESIAN_POINT('',(-7.3,-3.06161699786838E-16,-2.5));
#56523=CARTESIAN_POINT('Origin',(22.7,0.,0.));
#56524=CARTESIAN_POINT('Origin',(-7.3,0.,0.));
#56525=CARTESIAN_POINT('',(-7.3,1.15470053837925,2.));
#56526=CARTESIAN_POINT('',(-7.3,2.3094010767585,1.33236321473148E-16));
#56527=CARTESIAN_POINT('',(-7.3,1.15470053837925,2.));
#56528=CARTESIAN_POINT('',(-7.3,-1.15470053837925,2.));
#56529=CARTESIAN_POINT('',(-7.3,-1.15470053837925,2.));
#56530=CARTESIAN_POINT('',(-7.3,-2.3094010767585,4.08864764769604E-16));
#56531=CARTESIAN_POINT('',(-7.3,-2.3094010767585,4.08864764769604E-16));
#56532=CARTESIAN_POINT('',(-7.3,-1.15470053837925,-2.));
#56533=CARTESIAN_POINT('',(-7.3,-1.15470053837925,-2.));
#56534=CARTESIAN_POINT('',(-7.3,1.15470053837925,-2.));
#56535=CARTESIAN_POINT('',(-7.3,1.15470053837925,-2.));
#56536=CARTESIAN_POINT('',(-7.3,2.3094010767585,1.33236321473148E-16));
#56537=CARTESIAN_POINT('Origin',(22.7,2.5,0.));
#56538=CARTESIAN_POINT('Origin',(2.85,2.5,0.));
#56539=CARTESIAN_POINT('Origin',(-2.3,2.065,0.));
#56540=CARTESIAN_POINT('Origin',(-4.8,-1.15470053837925,2.));
#56541=CARTESIAN_POINT('',(-4.8,-1.15470053837925,2.));
#56542=CARTESIAN_POINT('',(-4.8,-1.15470053837925,2.));
#56543=CARTESIAN_POINT('',(-4.8,-1.15470053837925,2.));
#56544=CARTESIAN_POINT('',(-4.8,1.15470053837925,2.));
#56545=CARTESIAN_POINT('',(-4.8,1.15470053837925,2.));
#56546=CARTESIAN_POINT('',(-4.8,-1.15470053837925,2.));
#56547=CARTESIAN_POINT('Origin',(-4.8,-2.3094010767585,4.08864764769604E-16));
#56548=CARTESIAN_POINT('',(-4.8,-2.3094010767585,4.08864764769604E-16));
#56549=CARTESIAN_POINT('',(-4.8,-2.3094010767585,4.08864764769604E-16));
#56550=CARTESIAN_POINT('',(-4.8,-2.3094010767585,4.08864764769604E-16));
#56551=CARTESIAN_POINT('',(-4.8,-2.3094010767585,4.08864764769604E-16));
#56552=CARTESIAN_POINT('Origin',(-4.8,-1.15470053837925,-2.));
#56553=CARTESIAN_POINT('',(-4.8,-1.15470053837925,-2.));
#56554=CARTESIAN_POINT('',(-4.8,-1.15470053837925,-2.));
#56555=CARTESIAN_POINT('',(-4.8,-1.15470053837925,-2.));
#56556=CARTESIAN_POINT('',(-4.8,-1.15470053837925,-2.));
#56557=CARTESIAN_POINT('Origin',(-4.8,1.15470053837925,-2.));
#56558=CARTESIAN_POINT('',(-4.8,1.15470053837925,-2.));
#56559=CARTESIAN_POINT('',(-4.8,1.15470053837925,-2.));
#56560=CARTESIAN_POINT('',(-4.8,1.15470053837925,-2.));
#56561=CARTESIAN_POINT('',(-4.8,1.15470053837925,-2.));
#56562=CARTESIAN_POINT('Origin',(-4.8,2.3094010767585,1.33236321473148E-16));
#56563=CARTESIAN_POINT('',(-4.8,2.3094010767585,1.33236321473148E-16));
#56564=CARTESIAN_POINT('',(-4.8,2.3094010767585,1.33236321473148E-16));
#56565=CARTESIAN_POINT('',(-4.8,2.3094010767585,1.33236321473148E-16));
#56566=CARTESIAN_POINT('',(-4.8,2.3094010767585,1.33236321473148E-16));
#56567=CARTESIAN_POINT('Origin',(-4.8,1.15470053837925,2.));
#56568=CARTESIAN_POINT('',(-4.8,1.15470053837925,2.));
#56569=CARTESIAN_POINT('',(-4.8,1.15470053837925,2.));
#56570=CARTESIAN_POINT('Origin',(-4.8,0.,0.));
#56571=CARTESIAN_POINT('Origin',(-4.8,0.,0.));
#56572=CARTESIAN_POINT('Origin',(-4.8,0.,0.));
#56573=CARTESIAN_POINT('Origin',(-4.8,0.,0.));
#56574=CARTESIAN_POINT('Origin',(-4.8,0.,0.));
#56575=CARTESIAN_POINT('Origin',(-4.8,0.,0.));
#56576=CARTESIAN_POINT('Origin',(-7.3,-2.80889253323697E-17,0.));
#56577=CARTESIAN_POINT('',(-1.,5.,-6.12323399573677E-16));
#56578=CARTESIAN_POINT('Origin',(-1.,-3.84779799073558E-18,0.));
#56579=CARTESIAN_POINT('',(0.,5.,-6.12323399573677E-16));
#56580=CARTESIAN_POINT('',(-7.3,5.,-6.12323399573677E-16));
#56581=CARTESIAN_POINT('Origin',(0.,0.,0.));
#56582=CARTESIAN_POINT('Origin',(-7.3,-2.80889253323697E-17,0.));
#56583=CARTESIAN_POINT('',(0.,2.5,-3.06161699786838E-16));
#56584=CARTESIAN_POINT('Origin',(0.,0.,0.));
#56585=CARTESIAN_POINT('',(-1.,2.5,-3.06161699786838E-16));
#56586=CARTESIAN_POINT('',(-7.3,2.5,-3.06161699786838E-16));
#56587=CARTESIAN_POINT('Origin',(-1.,-3.84779799073558E-18,0.));
#56588=CARTESIAN_POINT('Origin',(-1.,5.,0.));
#56589=CARTESIAN_POINT('Origin',(-3.54259174671033E-17,5.,0.));
#56590=CARTESIAN_POINT('Origin',(-2.3,-2.80889253323697E-17,0.));
#56591=CARTESIAN_POINT('',(-1.,1.065,4.11439849795812));
#56592=CARTESIAN_POINT('',(-1.,-1.065,4.11439849795812));
#56593=CARTESIAN_POINT('Origin',(-1.,-1.22125762314651E-17,0.));
#56594=CARTESIAN_POINT('',(-2.3,-1.065,4.11439849795812));
#56595=CARTESIAN_POINT('',(-2.3,-1.065,4.11439849795812));
#56596=CARTESIAN_POINT('',(-2.3,1.065,4.11439849795812));
#56597=CARTESIAN_POINT('Origin',(-2.3,-2.80889253323697E-17,0.));
#56598=CARTESIAN_POINT('',(-2.3,1.065,4.11439849795812));
#56599=CARTESIAN_POINT('Origin',(-2.3,-2.80889253323697E-17,0.));
#56600=CARTESIAN_POINT('',(-1.,1.065,2.26180790519443));
#56601=CARTESIAN_POINT('',(-1.,-1.065,2.26180790519443));
#56602=CARTESIAN_POINT('Origin',(-1.,-1.22125762314651E-17,0.));
#56603=CARTESIAN_POINT('',(-2.3,1.065,2.26180790519443));
#56604=CARTESIAN_POINT('',(-2.3,1.065,2.26180790519443));
#56605=CARTESIAN_POINT('',(-2.3,-1.065,2.26180790519443));
#56606=CARTESIAN_POINT('Origin',(-2.3,-2.80889253323697E-17,0.));
#56607=CARTESIAN_POINT('',(-2.3,-1.065,2.26180790519443));
#56608=CARTESIAN_POINT('Origin',(-2.3,4.25,0.));
#56609=CARTESIAN_POINT('',(-2.3,-1.065,4.11439849795812));
#56610=CARTESIAN_POINT('',(-2.3,1.065,4.11439849795812));
#56611=CARTESIAN_POINT('Origin',(-1.,4.25,0.));
#56612=CARTESIAN_POINT('',(-1.,-1.065,4.11439849795812));
#56613=CARTESIAN_POINT('',(-1.,1.065,4.11439849795812));
#56614=CARTESIAN_POINT('Origin',(-2.3,1.065,4.11439849795812));
#56615=CARTESIAN_POINT('Origin',(-2.3,-1.065,4.11439849795812));
#57035=UNCERTAINTY_MEASURE_WITH_UNIT(LENGTH_MEASURE(0.01),#57080,
'DISTANCE_ACCURACY_VALUE',
'Maximum model space distance between geometric entities at asserted c
onnectivities');
#57040=UNCERTAINTY_MEASURE_WITH_UNIT(LENGTH_MEASURE(0.01),#57080,
'DISTANCE_ACCURACY_VALUE',
'Maximum model space distance between geometric entities at asserted c
onnectivities');
#57074=(
GEOMETRIC_REPRESENTATION_CONTEXT(3)
GLOBAL_UNCERTAINTY_ASSIGNED_CONTEXT((#57035))
GLOBAL_UNIT_ASSIGNED_CONTEXT((#57080,#57082,#57083))
REPRESENTATION_CONTEXT('','3D')
);
#57079=(
GEOMETRIC_REPRESENTATION_CONTEXT(3)
GLOBAL_UNCERTAINTY_ASSIGNED_CONTEXT((#57040))
GLOBAL_UNIT_ASSIGNED_CONTEXT((#57080,#57082,#57083))
REPRESENTATION_CONTEXT('','3D')
);
#57080=(
LENGTH_UNIT()
NAMED_UNIT(*)
SI_UNIT(.MILLI.,.METRE.)
);
#57082=(
NAMED_UNIT(*)
PLANE_ANGLE_UNIT()
SI_UNIT($,.RADIAN.)
);
#57083=(
NAMED_UNIT(*)
SI_UNIT($,.STERADIAN.)
SOLID_ANGLE_UNIT()
);
#57117=SHAPE_DEFINITION_REPRESENTATION(#57181,#57282);
#57181=PRODUCT_DEFINITION_SHAPE('',$,#57321);
#57282=SHAPE_REPRESENTATION('',(#27238),#57074);
#57287=PRODUCT_DEFINITION_CONTEXT('part definition',#57403,'design');
#57321=PRODUCT_DEFINITION('Low Head Cap Screw M5x25',
'Low Head Cap Screw M5x25',#57359,#57287);
#57359=PRODUCT_DEFINITION_FORMATION('',$,#57438);
#57403=APPLICATION_CONTEXT(
'Core Data for Automotive Mechanical Design Process');
#57404=PRODUCT_CONTEXT('part definition',#57403,'mechanical');
#57438=PRODUCT('Low Head Cap Screw M5x25','Low Head Cap Screw M5x25',$,
(#57404));
#57444=PRESENTATION_STYLE_ASSIGNMENT((#57446));
#57446=SURFACE_STYLE_USAGE(.BOTH.,#57448);
#57448=SURFACE_SIDE_STYLE('',(#57450));
#57450=SURFACE_STYLE_FILL_AREA(#57452);
#57452=FILL_AREA_STYLE('Opaque(202,209,238)',(#57454));
#57454=FILL_AREA_STYLE_COLOUR('Opaque(202,209,238)',#57456);
#57456=COLOUR_RGB('Opaque(202,209,238)',0.792156862745098,0.819607843137255,
0.933333333333333);
ENDSEC;
END-ISO-10303-21;
